ISO-10303-21;
HEADER;
/* Generated by software containing ST-Developer
 * from STEP Tools, Inc. (www.steptools.com) 
 */

FILE_DESCRIPTION(
/* description */ ('Bin tilter linkage'),
/* implementation_level */ '2;1');

FILE_NAME(
/* name */ 'M4 short cap screw (22).step',
/* time_stamp */ '2026-10-28T03:26:24-07:00',
/* author */ (''),
/* organization */ (''),
/* preprocessor_version */ 'ST-DEVELOPER v20.2',
/* originating_system */ 'Autodesk Translation Framework v15.17.0.0',
/* authorisation */ '');

FILE_SCHEMA (('AUTOMOTIVE_DESIGN { 1 0 10303 214 3 1 1 }'));
ENDSEC;

DATA;
#10=MECHANICAL_DESIGN_GEOMETRIC_PRESENTATION_REPRESENTATION('',(#922),#23728);
#710=SHAPE_REPRESENTATION_RELATIONSHIP('SRR','None',#24176,#816);
#816=ADVANCED_BREP_SHAPE_REPRESENTATION('',(#1035),#23676);
#922=STYLED_ITEM('',(#24772),#1035);
#1035=MANIFOLD_SOLID_BREP('Body1',#12453);
#1356=FACE_BOUND('',#3376,.T.);
#1703=PLANE('',#14632);
#1704=PLANE('',#14637);
#1705=PLANE('',#14640);
#2329=FACE_OUTER_BOUND('',#3375,.T.);
#2330=FACE_OUTER_BOUND('',#3377,.T.);
#2331=FACE_OUTER_BOUND('',#3378,.T.);
#2332=FACE_OUTER_BOUND('',#3379,.T.);
#2333=FACE_OUTER_BOUND('',#3380,.T.);
#3375=EDGE_LOOP('',(#10021));
#3376=EDGE_LOOP('',(#10022));
#3377=EDGE_LOOP('',(#10023,#10024,#10025,#10026));
#3378=EDGE_LOOP('',(#10027));
#3379=EDGE_LOOP('',(#10028,#10029,#10030,#10031));
#3380=EDGE_LOOP('',(#10032));
#4221=LINE('',#21629,#4896);
#4222=LINE('',#21633,#4897);
#4896=VECTOR('',#17768,0.350000000000001);
#4897=VECTOR('',#17773,0.199999999999999);
#5651=CIRCLE('',#14633,0.350000000000001);
#5652=CIRCLE('',#14634,0.199999999999999);
#5653=CIRCLE('',#14636,0.350000000000001);
#5654=CIRCLE('',#14639,0.199999999999999);
#6505=VERTEX_POINT('',#21622);
#6506=VERTEX_POINT('',#21624);
#6507=VERTEX_POINT('',#21627);
#6508=VERTEX_POINT('',#21632);
#7750=EDGE_CURVE('',#6505,#6505,#5651,.T.);
#7751=EDGE_CURVE('',#6506,#6506,#5652,.T.);
#7752=EDGE_CURVE('',#6507,#6507,#5653,.T.);
#7753=EDGE_CURVE('',#6507,#6505,#4221,.T.);
#7754=EDGE_CURVE('',#6506,#6508,#4222,.T.);
#7755=EDGE_CURVE('',#6508,#6508,#5654,.T.);
#10021=ORIENTED_EDGE('',*,*,#7750,.F.);
#10022=ORIENTED_EDGE('',*,*,#7751,.T.);
#10023=ORIENTED_EDGE('',*,*,#7752,.F.);
#10024=ORIENTED_EDGE('',*,*,#7753,.T.);
#10025=ORIENTED_EDGE('',*,*,#7750,.T.);
#10026=ORIENTED_EDGE('',*,*,#7753,.F.);
#10027=ORIENTED_EDGE('',*,*,#7752,.T.);
#10028=ORIENTED_EDGE('',*,*,#7751,.F.);
#10029=ORIENTED_EDGE('',*,*,#7754,.T.);
#10030=ORIENTED_EDGE('',*,*,#7755,.T.);
#10031=ORIENTED_EDGE('',*,*,#7754,.F.);
#10032=ORIENTED_EDGE('',*,*,#7755,.F.);
#11491=CYLINDRICAL_SURFACE('',#14635,0.350000000000001);
#11492=CYLINDRICAL_SURFACE('',#14638,0.199999999999999);
#12054=ADVANCED_FACE('',(#2329,#1356),#1703,.F.);
#12055=ADVANCED_FACE('',(#2330),#11491,.T.);
#12056=ADVANCED_FACE('',(#2331),#1704,.T.);
#12057=ADVANCED_FACE('',(#2332),#11492,.T.);
#12058=ADVANCED_FACE('',(#2333),#1705,.F.);
#12453=CLOSED_SHELL('',(#12054,#12055,#12056,#12057,#12058));
#14631=AXIS2_PLACEMENT_3D('',#21620,#17756,#17757);
#14632=AXIS2_PLACEMENT_3D('',#21621,#17758,#17759);
#14633=AXIS2_PLACEMENT_3D('',#21623,#17760,#17761);
#14634=AXIS2_PLACEMENT_3D('',#21625,#17762,#17763);
#14635=AXIS2_PLACEMENT_3D('',#21626,#17764,#17765);
#14636=AXIS2_PLACEMENT_3D('',#21628,#17766,#17767);
#14637=AXIS2_PLACEMENT_3D('',#21630,#17769,#17770);
#14638=AXIS2_PLACEMENT_3D('',#21631,#17771,#17772);
#14639=AXIS2_PLACEMENT_3D('',#21634,#17774,#17775);
#14640=AXIS2_PLACEMENT_3D('',#21635,#17776,#17777);
#17756=DIRECTION('axis',(0.,0.,1.));
#17757=DIRECTION('refdir',(1.,0.,0.));
#17758=DIRECTION('center_axis',(0.,1.,0.));
#17759=DIRECTION('ref_axis',(1.,0.,0.));
#17760=DIRECTION('center_axis',(0.,1.,0.));
#17761=DIRECTION('ref_axis',(1.,0.,0.));
#17762=DIRECTION('center_axis',(0.,1.,0.));
#17763=DIRECTION('ref_axis',(1.,0.,0.));
#17764=DIRECTION('center_axis',(0.,1.,0.));
#17765=DIRECTION('ref_axis',(1.,0.,0.));
#17766=DIRECTION('center_axis',(0.,1.,0.));
#17767=DIRECTION('ref_axis',(1.,0.,0.));
#17768=DIRECTION('',(0.,-1.,0.));
#17769=DIRECTION('center_axis',(0.,1.,0.));
#17770=DIRECTION('ref_axis',(1.,0.,0.));
#17771=DIRECTION('center_axis',(0.,1.,0.));
#17772=DIRECTION('ref_axis',(1.,0.,0.));
#17773=DIRECTION('',(0.,-1.,0.));
#17774=DIRECTION('center_axis',(0.,1.,0.));
#17775=DIRECTION('ref_axis',(1.,0.,0.));
#17776=DIRECTION('center_axis',(0.,1.,0.));
#17777=DIRECTION('ref_axis',(1.,0.,0.));
#21620=CARTESIAN_POINT('',(0.,0.,0.));
#21621=CARTESIAN_POINT('Origin',(16.6918524548049,0.8,13.6918524548049));
#21622=CARTESIAN_POINT('',(16.3418524548049,0.8,13.6918524548049));
#21623=CARTESIAN_POINT('Origin',(16.6918524548049,0.8,13.6918524548049));
#21624=CARTESIAN_POINT('',(16.4918524548049,0.8,13.6918524548049));
#21625=CARTESIAN_POINT('Origin',(16.6918524548049,0.8,13.6918524548049));
#21626=CARTESIAN_POINT('Origin',(16.6918524548049,0.8,13.6918524548049));
#21627=CARTESIAN_POINT('',(16.3418524548049,1.2,13.6918524548049));
#21628=CARTESIAN_POINT('Origin',(16.6918524548049,1.2,13.6918524548049));
#21629=CARTESIAN_POINT('',(16.3418524548049,0.8,13.6918524548049));
#21630=CARTESIAN_POINT('Origin',(16.6918524548049,1.2,13.6918524548049));
#21631=CARTESIAN_POINT('Origin',(16.6918524548049,0.1,13.6918524548049));
#21632=CARTESIAN_POINT('',(16.4918524548049,0.1,13.6918524548049));
#21633=CARTESIAN_POINT('',(16.4918524548049,0.1,13.6918524548049));
#21634=CARTESIAN_POINT('Origin',(16.6918524548049,0.1,13.6918524548049));
#21635=CARTESIAN_POINT('Origin',(16.6918524548049,0.1,13.6918524548049));
#23559=UNCERTAINTY_MEASURE_WITH_UNIT(LENGTH_MEASURE(0.001),#23729,
'DISTANCE_ACCURACY_VALUE',
'Maximum model space distance between geometric entities at asserted c
onnectivities');
#23611=UNCERTAINTY_MEASURE_WITH_UNIT(LENGTH_MEASURE(0.001),#23729,
'DISTANCE_ACCURACY_VALUE',
'Maximum model space distance between geometric entities at asserted c
onnectivities');
#23676=(
GEOMETRIC_REPRESENTATION_CONTEXT(3)
GLOBAL_UNCERTAINTY_ASSIGNED_CONTEXT((#23559))
GLOBAL_UNIT_ASSIGNED_CONTEXT((#23729,#23731,#23732))
REPRESENTATION_CONTEXT('','3D')
);
#23728=(
GEOMETRIC_REPRESENTATION_CONTEXT(3)
GLOBAL_UNCERTAINTY_ASSIGNED_CONTEXT((#23611))
GLOBAL_UNIT_ASSIGNED_CONTEXT((#23729,#23731,#23732))
REPRESENTATION_CONTEXT('','3D')
);
#23729=(
LENGTH_UNIT()
NAMED_UNIT(*)
SI_UNIT(.CENTI.,.METRE.)
);
#23731=(
NAMED_UNIT(*)
PLANE_ANGLE_UNIT()
SI_UNIT($,.RADIAN.)
);
#23732=(
NAMED_UNIT(*)
SI_UNIT($,.STERADIAN.)
SOLID_ANGLE_UNIT()
);
#23797=SHAPE_DEFINITION_REPRESENTATION(#23913,#24176);
#23913=PRODUCT_DEFINITION_SHAPE('',$,#24293);
#24176=SHAPE_REPRESENTATION('',(#14631),#23676);
#24228=PRODUCT_DEFINITION_CONTEXT('part definition',#24578,'design');
#24293=PRODUCT_DEFINITION('M4 short cap screw (22)',
'M4 short cap screw (22)',#24409,#24228);
#24409=PRODUCT_DEFINITION_FORMATION('',$,#24644);
#24578=APPLICATION_CONTEXT(
'Core Data for Automotive Mechanical Design Process');
#24579=PRODUCT_CONTEXT('part definition',#24578,'mechanical');
#24644=PRODUCT('M4 short cap screw (22)','M4 short cap screw (22)',
'M4 short cap screw (22)',(#24579));
#24766=COLOUR_RGB('Black',0.12,0.14,0.17);
#24767=FILL_AREA_STYLE_COLOUR('',#24766);
#24768=FILL_AREA_STYLE('',(#24767));
#24769=SURFACE_STYLE_FILL_AREA(#24768);
#24770=SURFACE_SIDE_STYLE('',(#24769));
#24771=SURFACE_STYLE_USAGE(.BOTH.,#24770);
#24772=PRESENTATION_STYLE_ASSIGNMENT((#24771));
ENDSEC;
END-ISO-10303-21;
